ISO-10303-21;
HEADER;
/* Generated by software containing ST-Developer
 * from STEP Tools, Inc. (www.steptools.com) 
 */

FILE_DESCRIPTION(
/* description */ ('Turntable on roller ring'),
/* implementation_level */ '2;1');

FILE_NAME(
/* name */ 'Outer race retainer (3).step',
/* time_stamp */ '2026-10-28T03:23:59-07:00',
/* author */ (''),
/* organization */ (''),
/* preprocessor_version */ 'ST-DEVELOPER v20.2',
/* originating_system */ 'Autodesk Translation Framework v15.17.0.0',
/* authorisation */ '');

FILE_SCHEMA (('AUTOMOTIVE_DESIGN { 1 0 10303 214 3 1 1 }'));
ENDSEC;

DATA;
#10=MECHANICAL_DESIGN_GEOMETRIC_PRESENTATION_REPRESENTATION('',(#669),#16281);
#550=SHAPE_REPRESENTATION_RELATIONSHIP('SRR','None',#16572,#605);
#605=ADVANCED_BREP_SHAPE_REPRESENTATION('',(#737),#16266);
#669=STYLED_ITEM('',(#16932),#737);
#737=MANIFOLD_SOLID_BREP('Body1',#8414);
#967=FACE_BOUND('',#2394,.T.);
#968=FACE_BOUND('',#2396,.T.);
#1219=PLANE('',#9982);
#1220=PLANE('',#9983);
#1676=FACE_OUTER_BOUND('',#2391,.T.);
#1677=FACE_OUTER_BOUND('',#2392,.T.);
#1678=FACE_OUTER_BOUND('',#2393,.T.);
#1679=FACE_OUTER_BOUND('',#2395,.T.);
#2391=EDGE_LOOP('',(#7373,#7374,#7375,#7376));
#2392=EDGE_LOOP('',(#7377,#7378,#7379,#7380));
#2393=EDGE_LOOP('',(#7381));
#2394=EDGE_LOOP('',(#7382));
#2395=EDGE_LOOP('',(#7383));
#2396=EDGE_LOOP('',(#7384));
#2946=LINE('',#15430,#3429);
#2947=LINE('',#15436,#3430);
#3429=VECTOR('',#12529,1.1);
#3430=VECTOR('',#12536,1.5);
#3849=CIRCLE('',#9977,1.1);
#3850=CIRCLE('',#9978,1.1);
#3851=CIRCLE('',#9980,1.5);
#3852=CIRCLE('',#9981,1.5);
#4525=VERTEX_POINT('',#15427);
#4526=VERTEX_POINT('',#15429);
#4527=VERTEX_POINT('',#15433);
#4528=VERTEX_POINT('',#15435);
#5497=EDGE_CURVE('',#4525,#4525,#3849,.T.);
#5498=EDGE_CURVE('',#4525,#4526,#2946,.T.);
#5499=EDGE_CURVE('',#4526,#4526,#3850,.T.);
#5500=EDGE_CURVE('',#4527,#4527,#3851,.T.);
#5501=EDGE_CURVE('',#4527,#4528,#2947,.T.);
#5502=EDGE_CURVE('',#4528,#4528,#3852,.T.);
#7373=ORIENTED_EDGE('',*,*,#5497,.F.);
#7374=ORIENTED_EDGE('',*,*,#5498,.T.);
#7375=ORIENTED_EDGE('',*,*,#5499,.T.);
#7376=ORIENTED_EDGE('',*,*,#5498,.F.);
#7377=ORIENTED_EDGE('',*,*,#5500,.F.);
#7378=ORIENTED_EDGE('',*,*,#5501,.T.);
#7379=ORIENTED_EDGE('',*,*,#5502,.T.);
#7380=ORIENTED_EDGE('',*,*,#5501,.F.);
#7381=ORIENTED_EDGE('',*,*,#5500,.T.);
#7382=ORIENTED_EDGE('',*,*,#5497,.T.);
#7383=ORIENTED_EDGE('',*,*,#5502,.F.);
#7384=ORIENTED_EDGE('',*,*,#5499,.F.);
#7827=CYLINDRICAL_SURFACE('',#9976,1.1);
#7828=CYLINDRICAL_SURFACE('',#9979,1.5);
#8279=ADVANCED_FACE('',(#1676),#7827,.F.);
#8280=ADVANCED_FACE('',(#1677),#7828,.T.);
#8281=ADVANCED_FACE('',(#1678,#967),#1219,.T.);
#8282=ADVANCED_FACE('',(#1679,#968),#1220,.F.);
#8414=CLOSED_SHELL('',(#8279,#8280,#8281,#8282));
#9975=AXIS2_PLACEMENT_3D('',#15425,#12523,#12524);
#9976=AXIS2_PLACEMENT_3D('',#15426,#12525,#12526);
#9977=AXIS2_PLACEMENT_3D('',#15428,#12527,#12528);
#9978=AXIS2_PLACEMENT_3D('',#15431,#12530,#12531);
#9979=AXIS2_PLACEMENT_3D('',#15432,#12532,#12533);
#9980=AXIS2_PLACEMENT_3D('',#15434,#12534,#12535);
#9981=AXIS2_PLACEMENT_3D('',#15437,#12537,#12538);
#9982=AXIS2_PLACEMENT_3D('',#15438,#12539,#12540);
#9983=AXIS2_PLACEMENT_3D('',#15439,#12541,#12542);
#12523=DIRECTION('axis',(0.,0.,1.));
#12524=DIRECTION('refdir',(1.,0.,0.));
#12525=DIRECTION('center_axis',(0.,1.,0.));
#12526=DIRECTION('ref_axis',(1.,0.,0.));
#12527=DIRECTION('center_axis',(0.,-1.,0.));
#12528=DIRECTION('ref_axis',(1.,0.,0.));
#12529=DIRECTION('',(0.,-1.,0.));
#12530=DIRECTION('center_axis',(0.,-1.,0.));
#12531=DIRECTION('ref_axis',(1.,0.,0.));
#12532=DIRECTION('center_axis',(0.,1.,0.));
#12533=DIRECTION('ref_axis',(1.,0.,0.));
#12534=DIRECTION('center_axis',(0.,1.,0.));
#12535=DIRECTION('ref_axis',(1.,0.,0.));
#12536=DIRECTION('',(0.,-1.,0.));
#12537=DIRECTION('center_axis',(0.,1.,0.));
#12538=DIRECTION('ref_axis',(1.,0.,0.));
#12539=DIRECTION('center_axis',(0.,1.,0.));
#12540=DIRECTION('ref_axis',(1.,0.,0.));
#12541=DIRECTION('center_axis',(0.,1.,0.));
#12542=DIRECTION('ref_axis',(1.,0.,0.));
#15425=CARTESIAN_POINT('',(0.,0.,0.));
#15426=CARTESIAN_POINT('Origin',(0.,15.45,3.5));
#15427=CARTESIAN_POINT('',(-1.1,15.65,3.5));
#15428=CARTESIAN_POINT('Origin',(0.,15.65,3.5));
#15429=CARTESIAN_POINT('',(-1.1,15.45,3.5));
#15430=CARTESIAN_POINT('',(-1.1,15.45,3.5));
#15431=CARTESIAN_POINT('Origin',(0.,15.45,3.5));
#15432=CARTESIAN_POINT('Origin',(0.,15.45,3.5));
#15433=CARTESIAN_POINT('',(-1.5,15.65,3.5));
#15434=CARTESIAN_POINT('Origin',(0.,15.65,3.5));
#15435=CARTESIAN_POINT('',(-1.5,15.45,3.5));
#15436=CARTESIAN_POINT('',(-1.5,15.45,3.5));
#15437=CARTESIAN_POINT('Origin',(0.,15.45,3.5));
#15438=CARTESIAN_POINT('Origin',(0.,15.65,3.5));
#15439=CARTESIAN_POINT('Origin',(0.,15.45,3.5));
#16197=UNCERTAINTY_MEASURE_WITH_UNIT(LENGTH_MEASURE(0.001),#16282,
'DISTANCE_ACCURACY_VALUE',
'Maximum model space distance between geometric entities at asserted c
onnectivities');
#16212=UNCERTAINTY_MEASURE_WITH_UNIT(LENGTH_MEASURE(0.001),#16282,
'DISTANCE_ACCURACY_VALUE',
'Maximum model space distance between geometric entities at asserted c
onnectivities');
#16266=(
GEOMETRIC_REPRESENTATION_CONTEXT(3)
GLOBAL_UNCERTAINTY_ASSIGNED_CONTEXT((#16197))
GLOBAL_UNIT_ASSIGNED_CONTEXT((#16282,#16284,#16285))
REPRESENTATION_CONTEXT('','3D')
);
#16281=(
GEOMETRIC_REPRESENTATION_CONTEXT(3)
GLOBAL_UNCERTAINTY_ASSIGNED_CONTEXT((#16212))
GLOBAL_UNIT_ASSIGNED_CONTEXT((#16282,#16284,#16285))
REPRESENTATION_CONTEXT('','3D')
);
#16282=(
LENGTH_UNIT()
NAMED_UNIT(*)
SI_UNIT(.CENTI.,.METRE.)
);
#16284=(
NAMED_UNIT(*)
PLANE_ANGLE_UNIT()
SI_UNIT($,.RADIAN.)
);
#16285=(
NAMED_UNIT(*)
SI_UNIT($,.STERADIAN.)
SOLID_ANGLE_UNIT()
);
#16339=SHAPE_DEFINITION_REPRESENTATION(#16473,#16572);
#16473=PRODUCT_DEFINITION_SHAPE('',$,#16641);
#16572=SHAPE_REPRESENTATION('',(#9975),#16266);
#16587=PRODUCT_DEFINITION_CONTEXT('part definition',#16793,'design');
#16641=PRODUCT_DEFINITION('Outer race retainer (3)',
'Outer race retainer (3)',#16709,#16587);
#16709=PRODUCT_DEFINITION_FORMATION('',$,#16848);
#16793=APPLICATION_CONTEXT(
'Core Data for Automotive Mechanical Design Process');
#16794=PRODUCT_CONTEXT('part definition',#16793,'mechanical');
#16848=PRODUCT('Outer race retainer (3)','Outer race retainer (3)',
'Outer race retainer (3)',(#16794));
#16926=COLOUR_RGB('Grey',0.48,0.52,0.57);
#16927=FILL_AREA_STYLE_COLOUR('',#16926);
#16928=FILL_AREA_STYLE('',(#16927));
#16929=SURFACE_STYLE_FILL_AREA(#16928);
#16930=SURFACE_SIDE_STYLE('',(#16929));
#16931=SURFACE_STYLE_USAGE(.BOTH.,#16930);
#16932=PRESENTATION_STYLE_ASSIGNMENT((#16931));
ENDSEC;
END-ISO-10303-21;
